ISO-10303-21;
HEADER;
/* Generated by software containing ST-Developer
 * from STEP Tools, Inc. (www.steptools.com) 
 */

FILE_DESCRIPTION(
/* description */ ('Independent bearing-supported roller-ramp one-way clutch. Six logarit
hmic ramps with plain solid rollers, sprung guided plungers, native Co
il variants, removable shared keepers, rounded parallel key, shaft wit
h complete retaining lips, bronze journal/thrust support and bolted co
vers. Native rotor, roller planar/spin and plunger joints permit manua
l geometric engaged/released inspection. Automatic frictional torque s
witching/contact dynamics are not simulated; no capacity, hardness, fi
t, lubrication, speed, force or life rating. External input driver/cou
pling/anchors outside assembly.'),
/* implementation_level */ '2;1');

FILE_NAME(
/* name */ 'Shaft thrust washer.step',
/* time_stamp */ '2026-11-08T07:04:38-08:00',
/* author */ (''),
/* organization */ (''),
/* preprocessor_version */ 'ST-DEVELOPER v20.2',
/* originating_system */ 'Autodesk Translation Framework v15.17.0.0',
/* authorisation */ '');

FILE_SCHEMA (('AUTOMOTIVE_DESIGN { 1 0 10303 214 3 1 1 }'));
ENDSEC;

DATA;
#10=MECHANICAL_DESIGN_GEOMETRIC_PRESENTATION_REPRESENTATION('',(#310),#99526);
#278=SHAPE_REPRESENTATION_RELATIONSHIP('SRR','None',#99635,#294);
#294=ADVANCED_BREP_SHAPE_REPRESENTATION('',(#326),#99520);
#310=STYLED_ITEM('',(#99717),#326);
#326=MANIFOLD_SOLID_BREP('Body1',#18280);
#434=FACE_BOUND('',#2676,.T.);
#435=FACE_BOUND('',#2678,.T.);
#583=PLANE('',#19619);
#584=PLANE('',#19620);
#1574=FACE_OUTER_BOUND('',#2673,.T.);
#1575=FACE_OUTER_BOUND('',#2674,.T.);
#1576=FACE_OUTER_BOUND('',#2675,.T.);
#1577=FACE_OUTER_BOUND('',#2677,.T.);
#2673=EDGE_LOOP('',(#16044,#16045,#16046,#16047));
#2674=EDGE_LOOP('',(#16048,#16049,#16050,#16051));
#2675=EDGE_LOOP('',(#16052));
#2676=EDGE_LOOP('',(#16053));
#2677=EDGE_LOOP('',(#16054));
#2678=EDGE_LOOP('',(#16055));
#3084=CIRCLE('',#19614,10.);
#3085=CIRCLE('',#19615,10.);
#3086=CIRCLE('',#19617,14.);
#3087=CIRCLE('',#19618,14.);
#5434=LINE('',#94884,#6338);
#5435=LINE('',#94890,#6339);
#6338=VECTOR('',#22907,10.);
#6339=VECTOR('',#22914,14.);
#8099=VERTEX_POINT('',#94881);
#8100=VERTEX_POINT('',#94883);
#8101=VERTEX_POINT('',#94887);
#8102=VERTEX_POINT('',#94889);
#10774=EDGE_CURVE('',#8099,#8099,#3084,.T.);
#10775=EDGE_CURVE('',#8099,#8100,#5434,.T.);
#10776=EDGE_CURVE('',#8100,#8100,#3085,.T.);
#10777=EDGE_CURVE('',#8101,#8101,#3086,.T.);
#10778=EDGE_CURVE('',#8101,#8102,#5435,.T.);
#10779=EDGE_CURVE('',#8102,#8102,#3087,.T.);
#16044=ORIENTED_EDGE('',*,*,#10774,.F.);
#16045=ORIENTED_EDGE('',*,*,#10775,.T.);
#16046=ORIENTED_EDGE('',*,*,#10776,.T.);
#16047=ORIENTED_EDGE('',*,*,#10775,.F.);
#16048=ORIENTED_EDGE('',*,*,#10777,.F.);
#16049=ORIENTED_EDGE('',*,*,#10778,.T.);
#16050=ORIENTED_EDGE('',*,*,#10779,.T.);
#16051=ORIENTED_EDGE('',*,*,#10778,.F.);
#16052=ORIENTED_EDGE('',*,*,#10777,.T.);
#16053=ORIENTED_EDGE('',*,*,#10774,.T.);
#16054=ORIENTED_EDGE('',*,*,#10779,.F.);
#16055=ORIENTED_EDGE('',*,*,#10776,.F.);
#17214=CYLINDRICAL_SURFACE('',#19613,10.);
#17215=CYLINDRICAL_SURFACE('',#19616,14.);
#18172=ADVANCED_FACE('',(#1574),#17214,.F.);
#18173=ADVANCED_FACE('',(#1575),#17215,.T.);
#18174=ADVANCED_FACE('',(#1576,#434),#583,.T.);
#18175=ADVANCED_FACE('',(#1577,#435),#584,.F.);
#18280=CLOSED_SHELL('',(#18172,#18173,#18174,#18175));
#19612=AXIS2_PLACEMENT_3D('',#94879,#22901,#22902);
#19613=AXIS2_PLACEMENT_3D('',#94880,#22903,#22904);
#19614=AXIS2_PLACEMENT_3D('',#94882,#22905,#22906);
#19615=AXIS2_PLACEMENT_3D('',#94885,#22908,#22909);
#19616=AXIS2_PLACEMENT_3D('',#94886,#22910,#22911);
#19617=AXIS2_PLACEMENT_3D('',#94888,#22912,#22913);
#19618=AXIS2_PLACEMENT_3D('',#94891,#22915,#22916);
#19619=AXIS2_PLACEMENT_3D('',#94892,#22917,#22918);
#19620=AXIS2_PLACEMENT_3D('',#94893,#22919,#22920);
#22901=DIRECTION('axis',(0.,0.,1.));
#22902=DIRECTION('refdir',(1.,0.,0.));
#22903=DIRECTION('center_axis',(0.,0.,1.));
#22904=DIRECTION('ref_axis',(1.,0.,0.));
#22905=DIRECTION('center_axis',(0.,0.,-1.));
#22906=DIRECTION('ref_axis',(1.,0.,0.));
#22907=DIRECTION('',(0.,0.,-1.));
#22908=DIRECTION('center_axis',(0.,0.,-1.));
#22909=DIRECTION('ref_axis',(1.,0.,0.));
#22910=DIRECTION('center_axis',(0.,0.,1.));
#22911=DIRECTION('ref_axis',(1.,0.,0.));
#22912=DIRECTION('center_axis',(0.,0.,1.));
#22913=DIRECTION('ref_axis',(1.,0.,0.));
#22914=DIRECTION('',(0.,0.,-1.));
#22915=DIRECTION('center_axis',(0.,0.,1.));
#22916=DIRECTION('ref_axis',(1.,0.,0.));
#22917=DIRECTION('center_axis',(0.,0.,1.));
#22918=DIRECTION('ref_axis',(1.,0.,0.));
#22919=DIRECTION('center_axis',(0.,0.,1.));
#22920=DIRECTION('ref_axis',(1.,0.,0.));
#94879=CARTESIAN_POINT('',(0.,0.,0.));
#94880=CARTESIAN_POINT('Origin',(0.,0.,0.));
#94881=CARTESIAN_POINT('',(-10.,-1.22464679914735E-15,2.));
#94882=CARTESIAN_POINT('Origin',(0.,0.,2.));
#94883=CARTESIAN_POINT('',(-10.,-1.22464679914735E-15,0.));
#94884=CARTESIAN_POINT('',(-10.,-1.22464679914735E-15,0.));
#94885=CARTESIAN_POINT('Origin',(0.,0.,0.));
#94886=CARTESIAN_POINT('Origin',(0.,0.,0.));
#94887=CARTESIAN_POINT('',(-14.,-1.71450551880629E-15,2.));
#94888=CARTESIAN_POINT('Origin',(0.,0.,2.));
#94889=CARTESIAN_POINT('',(-14.,-1.71450551880629E-15,0.));
#94890=CARTESIAN_POINT('',(-14.,-1.71450551880629E-15,0.));
#94891=CARTESIAN_POINT('Origin',(0.,0.,0.));
#94892=CARTESIAN_POINT('Origin',(0.,0.,2.));
#94893=CARTESIAN_POINT('Origin',(0.,0.,0.));
#99502=UNCERTAINTY_MEASURE_WITH_UNIT(LENGTH_MEASURE(0.01),#99527,
'DISTANCE_ACCURACY_VALUE',
'Maximum model space distance between geometric entities at asserted c
onnectivities');
#99508=UNCERTAINTY_MEASURE_WITH_UNIT(LENGTH_MEASURE(0.01),#99527,
'DISTANCE_ACCURACY_VALUE',
'Maximum model space distance between geometric entities at asserted c
onnectivities');
#99520=(
GEOMETRIC_REPRESENTATION_CONTEXT(3)
GLOBAL_UNCERTAINTY_ASSIGNED_CONTEXT((#99502))
GLOBAL_UNIT_ASSIGNED_CONTEXT((#99527,#99529,#99530))
REPRESENTATION_CONTEXT('','3D')
);
#99526=(
GEOMETRIC_REPRESENTATION_CONTEXT(3)
GLOBAL_UNCERTAINTY_ASSIGNED_CONTEXT((#99508))
GLOBAL_UNIT_ASSIGNED_CONTEXT((#99527,#99529,#99530))
REPRESENTATION_CONTEXT('','3D')
);
#99527=(
LENGTH_UNIT()
NAMED_UNIT(*)
SI_UNIT(.MILLI.,.METRE.)
);
#99529=(
NAMED_UNIT(*)
PLANE_ANGLE_UNIT()
SI_UNIT($,.RADIAN.)
);
#99530=(
NAMED_UNIT(*)
SI_UNIT($,.STERADIAN.)
SOLID_ANGLE_UNIT()
);
#99542=SHAPE_DEFINITION_REPRESENTATION(#99559,#99635);
#99559=PRODUCT_DEFINITION_SHAPE('',$,#99653);
#99635=SHAPE_REPRESENTATION('',(#19612),#99520);
#99641=PRODUCT_DEFINITION_CONTEXT('part definition',#99694,'design');
#99653=PRODUCT_DEFINITION('Shaft thrust washer','Shaft thrust washer',#99670,
#99641);
#99670=PRODUCT_DEFINITION_FORMATION('',$,#99707);
#99694=APPLICATION_CONTEXT(
'Core Data for Automotive Mechanical Design Process');
#99695=PRODUCT_CONTEXT('part definition',#99694,'mechanical');
#99707=PRODUCT('Shaft thrust washer','Shaft thrust washer',$,(#99695));
#99717=PRESENTATION_STYLE_ASSIGNMENT((#99730));
#99730=SURFACE_STYLE_USAGE(.BOTH.,#99743);
#99743=SURFACE_SIDE_STYLE('',(#99756));
#99756=SURFACE_STYLE_FILL_AREA(#99769);
#99769=FILL_AREA_STYLE('Light gray',(#99782));
#99782=FILL_AREA_STYLE_COLOUR('Light gray',#99795);
#99795=COLOUR_RGB('Light gray',0.725490196078431,0.752941176470588,0.792156862745098);
ENDSEC;
END-ISO-10303-21;
